ISO-10303-21;
HEADER;
/* Generated by software containing ST-Developer
 * from STEP Tools, Inc. (www.steptools.com) 
 */

FILE_DESCRIPTION(
/* description */ ('Double-row support with tensioned shaft'),
/* implementation_level */ '2;1');

FILE_NAME(
/* name */ 'Flange hole reducer (5).step',
/* time_stamp */ '2026-10-27T10:50:35-07:00',
/* author */ (''),
/* organization */ (''),
/* preprocessor_version */ 'ST-DEVELOPER v20.2',
/* originating_system */ 'Autodesk Translation Framework v15.17.0.0',
/* authorisation */ '');

FILE_SCHEMA (('AUTOMOTIVE_DESIGN { 1 0 10303 214 3 1 1 }'));
ENDSEC;

DATA;
#10=MECHANICAL_DESIGN_GEOMETRIC_PRESENTATION_REPRESENTATION('',(#491),#11559);
#427=SHAPE_REPRESENTATION_RELATIONSHIP('SRR','None',#11735,#459);
#459=ADVANCED_BREP_SHAPE_REPRESENTATION('',(#524),#11537);
#491=STYLED_ITEM('',(#11981),#524);
#524=MANIFOLD_SOLID_BREP('Body1',#6336);
#604=FACE_BOUND('',#1418,.T.);
#605=FACE_BOUND('',#1420,.T.);
#735=PLANE('',#6898);
#736=PLANE('',#6899);
#1009=FACE_OUTER_BOUND('',#1415,.T.);
#1010=FACE_OUTER_BOUND('',#1416,.T.);
#1011=FACE_OUTER_BOUND('',#1417,.T.);
#1012=FACE_OUTER_BOUND('',#1419,.T.);
#1415=EDGE_LOOP('',(#4738,#4739,#4740,#4741));
#1416=EDGE_LOOP('',(#4742,#4743,#4744,#4745));
#1417=EDGE_LOOP('',(#4746));
#1418=EDGE_LOOP('',(#4747));
#1419=EDGE_LOOP('',(#4748));
#1420=EDGE_LOOP('',(#4749));
#1874=LINE('',#9685,#2421);
#1875=LINE('',#9691,#2422);
#2421=VECTOR('',#7865,0.425);
#2422=VECTOR('',#7872,0.595);
#2908=CIRCLE('',#6893,0.425);
#2909=CIRCLE('',#6894,0.425);
#2910=CIRCLE('',#6896,0.595);
#2911=CIRCLE('',#6897,0.595);
#3163=VERTEX_POINT('',#9682);
#3164=VERTEX_POINT('',#9684);
#3165=VERTEX_POINT('',#9688);
#3166=VERTEX_POINT('',#9690);
#3754=EDGE_CURVE('',#3163,#3163,#2908,.T.);
#3755=EDGE_CURVE('',#3163,#3164,#1874,.T.);
#3756=EDGE_CURVE('',#3164,#3164,#2909,.T.);
#3757=EDGE_CURVE('',#3165,#3165,#2910,.T.);
#3758=EDGE_CURVE('',#3165,#3166,#1875,.T.);
#3759=EDGE_CURVE('',#3166,#3166,#2911,.T.);
#4738=ORIENTED_EDGE('',*,*,#3754,.F.);
#4739=ORIENTED_EDGE('',*,*,#3755,.T.);
#4740=ORIENTED_EDGE('',*,*,#3756,.T.);
#4741=ORIENTED_EDGE('',*,*,#3755,.F.);
#4742=ORIENTED_EDGE('',*,*,#3757,.F.);
#4743=ORIENTED_EDGE('',*,*,#3758,.T.);
#4744=ORIENTED_EDGE('',*,*,#3759,.T.);
#4745=ORIENTED_EDGE('',*,*,#3758,.F.);
#4746=ORIENTED_EDGE('',*,*,#3757,.T.);
#4747=ORIENTED_EDGE('',*,*,#3754,.T.);
#4748=ORIENTED_EDGE('',*,*,#3759,.F.);
#4749=ORIENTED_EDGE('',*,*,#3756,.F.);
#5926=CYLINDRICAL_SURFACE('',#6892,0.425);
#5927=CYLINDRICAL_SURFACE('',#6895,0.595);
#6072=ADVANCED_FACE('',(#1009),#5926,.F.);
#6073=ADVANCED_FACE('',(#1010),#5927,.T.);
#6074=ADVANCED_FACE('',(#1011,#604),#735,.T.);
#6075=ADVANCED_FACE('',(#1012,#605),#736,.F.);
#6336=CLOSED_SHELL('',(#6072,#6073,#6074,#6075));
#6891=AXIS2_PLACEMENT_3D('',#9680,#7859,#7860);
#6892=AXIS2_PLACEMENT_3D('',#9681,#7861,#7862);
#6893=AXIS2_PLACEMENT_3D('',#9683,#7863,#7864);
#6894=AXIS2_PLACEMENT_3D('',#9686,#7866,#7867);
#6895=AXIS2_PLACEMENT_3D('',#9687,#7868,#7869);
#6896=AXIS2_PLACEMENT_3D('',#9689,#7870,#7871);
#6897=AXIS2_PLACEMENT_3D('',#9692,#7873,#7874);
#6898=AXIS2_PLACEMENT_3D('',#9693,#7875,#7876);
#6899=AXIS2_PLACEMENT_3D('',#9694,#7877,#7878);
#7859=DIRECTION('axis',(0.,0.,1.));
#7860=DIRECTION('refdir',(1.,0.,0.));
#7861=DIRECTION('center_axis',(0.,1.,0.));
#7862=DIRECTION('ref_axis',(1.,0.,0.));
#7863=DIRECTION('center_axis',(0.,-1.,0.));
#7864=DIRECTION('ref_axis',(1.,0.,0.));
#7865=DIRECTION('',(0.,-1.,0.));
#7866=DIRECTION('center_axis',(0.,-1.,0.));
#7867=DIRECTION('ref_axis',(1.,0.,0.));
#7868=DIRECTION('center_axis',(0.,1.,0.));
#7869=DIRECTION('ref_axis',(1.,0.,0.));
#7870=DIRECTION('center_axis',(0.,1.,0.));
#7871=DIRECTION('ref_axis',(1.,0.,0.));
#7872=DIRECTION('',(0.,-1.,0.));
#7873=DIRECTION('center_axis',(0.,1.,0.));
#7874=DIRECTION('ref_axis',(1.,0.,0.));
#7875=DIRECTION('center_axis',(0.,1.,0.));
#7876=DIRECTION('ref_axis',(1.,0.,0.));
#7877=DIRECTION('center_axis',(0.,1.,0.));
#7878=DIRECTION('ref_axis',(1.,0.,0.));
#9680=CARTESIAN_POINT('',(0.,0.,0.));
#9681=CARTESIAN_POINT('Origin',(-3.2,17.5,13.2));
#9682=CARTESIAN_POINT('',(-3.625,18.5,13.2));
#9683=CARTESIAN_POINT('Origin',(-3.2,18.5,13.2));
#9684=CARTESIAN_POINT('',(-3.625,17.5,13.2));
#9685=CARTESIAN_POINT('',(-3.625,17.5,13.2));
#9686=CARTESIAN_POINT('Origin',(-3.2,17.5,13.2));
#9687=CARTESIAN_POINT('Origin',(-3.2,17.5,13.2));
#9688=CARTESIAN_POINT('',(-3.795,18.5,13.2));
#9689=CARTESIAN_POINT('Origin',(-3.2,18.5,13.2));
#9690=CARTESIAN_POINT('',(-3.795,17.5,13.2));
#9691=CARTESIAN_POINT('',(-3.795,17.5,13.2));
#9692=CARTESIAN_POINT('Origin',(-3.2,17.5,13.2));
#9693=CARTESIAN_POINT('Origin',(-3.2,18.5,13.2));
#9694=CARTESIAN_POINT('Origin',(-3.2,17.5,13.2));
#11500=UNCERTAINTY_MEASURE_WITH_UNIT(LENGTH_MEASURE(0.001),#11560,
'DISTANCE_ACCURACY_VALUE',
'Maximum model space distance between geometric entities at asserted c
onnectivities');
#11522=UNCERTAINTY_MEASURE_WITH_UNIT(LENGTH_MEASURE(0.001),#11560,
'DISTANCE_ACCURACY_VALUE',
'Maximum model space distance between geometric entities at asserted c
onnectivities');
#11537=(
GEOMETRIC_REPRESENTATION_CONTEXT(3)
GLOBAL_UNCERTAINTY_ASSIGNED_CONTEXT((#11500))
GLOBAL_UNIT_ASSIGNED_CONTEXT((#11560,#11562,#11563))
REPRESENTATION_CONTEXT('','3D')
);
#11559=(
GEOMETRIC_REPRESENTATION_CONTEXT(3)
GLOBAL_UNCERTAINTY_ASSIGNED_CONTEXT((#11522))
GLOBAL_UNIT_ASSIGNED_CONTEXT((#11560,#11562,#11563))
REPRESENTATION_CONTEXT('','3D')
);
#11560=(
LENGTH_UNIT()
NAMED_UNIT(*)
SI_UNIT(.CENTI.,.METRE.)
);
#11562=(
NAMED_UNIT(*)
PLANE_ANGLE_UNIT()
SI_UNIT($,.RADIAN.)
);
#11563=(
NAMED_UNIT(*)
SI_UNIT($,.STERADIAN.)
SOLID_ANGLE_UNIT()
);
#11578=SHAPE_DEFINITION_REPRESENTATION(#11614,#11735);
#11614=PRODUCT_DEFINITION_SHAPE('',$,#11772);
#11735=SHAPE_REPRESENTATION('',(#6891),#11537);
#11757=PRODUCT_DEFINITION_CONTEXT('part definition',#11867,'design');
#11772=PRODUCT_DEFINITION('Flange hole reducer (5)',
'Flange hole reducer (5)',#11808,#11757);
#11808=PRODUCT_DEFINITION_FORMATION('',$,#11883);
#11867=APPLICATION_CONTEXT(
'Core Data for Automotive Mechanical Design Process');
#11868=PRODUCT_CONTEXT('part definition',#11867,'mechanical');
#11883=PRODUCT('Flange hole reducer (5)','Flange hole reducer (5)',
'Flange hole reducer (5)',(#11868));
#11975=COLOUR_RGB('Off White',0.89,0.88,0.83);
#11976=FILL_AREA_STYLE_COLOUR('',#11975);
#11977=FILL_AREA_STYLE('',(#11976));
#11978=SURFACE_STYLE_FILL_AREA(#11977);
#11979=SURFACE_SIDE_STYLE('',(#11978));
#11980=SURFACE_STYLE_USAGE(.BOTH.,#11979);
#11981=PRESENTATION_STYLE_ASSIGNMENT((#11980));
ENDSEC;
END-ISO-10303-21;
